ISO-10303-21;
HEADER;
/* Generated by software containing ST-Developer
 * from STEP Tools, Inc. (www.steptools.com) 
 */

FILE_DESCRIPTION(
/* description */ ('STEP AP214'),
/* implementation_level */ '2;1');

FILE_NAME(
/* name */ 'PRT-TQ-1012-07.step',
/* time_stamp */ '2026-10-07T12:49:37-07:00',
/* author */ (''),
/* organization */ (''),
/* preprocessor_version */ 'ST-DEVELOPER v20.2',
/* originating_system */ 'Autodesk Translation Framework v15.15.0.0',
/* authorisation */ '');

FILE_SCHEMA (('AUTOMOTIVE_DESIGN { 1 0 10303 214 3 1 1 }'));
ENDSEC;

DATA;
#10=MECHANICAL_DESIGN_GEOMETRIC_PRESENTATION_REPRESENTATION('',(#305),#33016);
#247=SHAPE_REPRESENTATION_RELATIONSHIP('SRR','None',#33141,#274);
#274=ADVANCED_BREP_SHAPE_REPRESENTATION('',(#332),#33002);
#305=STYLED_ITEM('',(#33288),#332);
#332=MANIFOLD_SOLID_BREP('Body1',#9956);
#520=FACE_BOUND('',#1961,.T.);
#521=FACE_BOUND('',#1967,.T.);
#926=PLANE('',#10836);
#927=PLANE('',#10837);
#928=PLANE('',#10838);
#929=PLANE('',#10839);
#930=PLANE('',#10840);
#931=PLANE('',#10841);
#932=PLANE('',#10842);
#933=PLANE('',#10843);
#934=PLANE('',#10844);
#935=PLANE('',#10845);
#936=PLANE('',#10846);
#937=PLANE('',#10847);
#938=PLANE('',#10848);
#939=PLANE('',#10849);
#940=PLANE('',#10850);
#941=PLANE('',#10851);
#942=PLANE('',#10852);
#943=PLANE('',#10853);
#944=PLANE('',#10854);
#945=PLANE('',#10855);
#946=PLANE('',#10856);
#947=PLANE('',#10857);
#948=PLANE('',#10858);
#949=PLANE('',#10859);
#950=PLANE('',#10860);
#951=PLANE('',#10861);
#952=PLANE('',#10862);
#953=PLANE('',#10863);
#954=PLANE('',#10864);
#955=PLANE('',#10865);
#956=PLANE('',#10866);
#957=PLANE('',#10867);
#1358=FACE_OUTER_BOUND('',#1960,.T.);
#1359=FACE_OUTER_BOUND('',#1962,.T.);
#1360=FACE_OUTER_BOUND('',#1963,.T.);
#1361=FACE_OUTER_BOUND('',#1964,.T.);
#1362=FACE_OUTER_BOUND('',#1965,.T.);
#1363=FACE_OUTER_BOUND('',#1966,.T.);
#1364=FACE_OUTER_BOUND('',#1968,.T.);
#1365=FACE_OUTER_BOUND('',#1969,.T.);
#1366=FACE_OUTER_BOUND('',#1970,.T.);
#1367=FACE_OUTER_BOUND('',#1971,.T.);
#1368=FACE_OUTER_BOUND('',#1972,.T.);
#1369=FACE_OUTER_BOUND('',#1973,.T.);
#1370=FACE_OUTER_BOUND('',#1974,.T.);
#1371=FACE_OUTER_BOUND('',#1975,.T.);
#1372=FACE_OUTER_BOUND('',#1976,.T.);
#1373=FACE_OUTER_BOUND('',#1977,.T.);
#1374=FACE_OUTER_BOUND('',#1978,.T.);
#1375=FACE_OUTER_BOUND('',#1979,.T.);
#1376=FACE_OUTER_BOUND('',#1980,.T.);
#1377=FACE_OUTER_BOUND('',#1981,.T.);
#1378=FACE_OUTER_BOUND('',#1982,.T.);
#1379=FACE_OUTER_BOUND('',#1983,.T.);
#1380=FACE_OUTER_BOUND('',#1984,.T.);
#1381=FACE_OUTER_BOUND('',#1985,.T.);
#1382=FACE_OUTER_BOUND('',#1986,.T.);
#1383=FACE_OUTER_BOUND('',#1987,.T.);
#1384=FACE_OUTER_BOUND('',#1988,.T.);
#1385=FACE_OUTER_BOUND('',#1989,.T.);
#1386=FACE_OUTER_BOUND('',#1990,.T.);
#1387=FACE_OUTER_BOUND('',#1991,.T.);
#1388=FACE_OUTER_BOUND('',#1992,.T.);
#1389=FACE_OUTER_BOUND('',#1993,.T.);
#1960=EDGE_LOOP('',(#8126,#8127,#8128,#8129));
#1961=EDGE_LOOP('',(#8130,#8131,#8132,#8133,#8134,#8135,#8136,#8137,#8138,
#8139,#8140,#8141));
#1962=EDGE_LOOP('',(#8142,#8143,#8144,#8145));
#1963=EDGE_LOOP('',(#8146,#8147,#8148,#8149));
#1964=EDGE_LOOP('',(#8150,#8151,#8152,#8153));
#1965=EDGE_LOOP('',(#8154,#8155,#8156,#8157));
#1966=EDGE_LOOP('',(#8158,#8159,#8160,#8161));
#1967=EDGE_LOOP('',(#8162,#8163,#8164,#8165,#8166,#8167,#8168,#8169,#8170,
#8171,#8172,#8173));
#1968=EDGE_LOOP('',(#8174,#8175,#8176,#8177));
#1969=EDGE_LOOP('',(#8178,#8179,#8180,#8181));
#1970=EDGE_LOOP('',(#8182,#8183,#8184,#8185));
#1971=EDGE_LOOP('',(#8186,#8187,#8188,#8189));
#1972=EDGE_LOOP('',(#8190,#8191,#8192,#8193));
#1973=EDGE_LOOP('',(#8194,#8195,#8196,#8197));
#1974=EDGE_LOOP('',(#8198,#8199,#8200,#8201));
#1975=EDGE_LOOP('',(#8202,#8203,#8204,#8205));
#1976=EDGE_LOOP('',(#8206,#8207,#8208,#8209));
#1977=EDGE_LOOP('',(#8210,#8211,#8212,#8213));
#1978=EDGE_LOOP('',(#8214,#8215,#8216,#8217));
#1979=EDGE_LOOP('',(#8218,#8219,#8220,#8221));
#1980=EDGE_LOOP('',(#8222,#8223,#8224,#8225,#8226,#8227,#8228,#8229,#8230,
#8231,#8232,#8233));
#1981=EDGE_LOOP('',(#8234,#8235,#8236,#8237));
#1982=EDGE_LOOP('',(#8238,#8239,#8240,#8241));
#1983=EDGE_LOOP('',(#8242,#8243,#8244,#8245));
#1984=EDGE_LOOP('',(#8246,#8247,#8248,#8249));
#1985=EDGE_LOOP('',(#8250,#8251,#8252,#8253));
#1986=EDGE_LOOP('',(#8254,#8255,#8256,#8257));
#1987=EDGE_LOOP('',(#8258,#8259,#8260,#8261));
#1988=EDGE_LOOP('',(#8262,#8263,#8264,#8265));
#1989=EDGE_LOOP('',(#8266,#8267,#8268,#8269));
#1990=EDGE_LOOP('',(#8270,#8271,#8272,#8273));
#1991=EDGE_LOOP('',(#8274,#8275,#8276,#8277));
#1992=EDGE_LOOP('',(#8278,#8279,#8280,#8281));
#1993=EDGE_LOOP('',(#8282,#8283,#8284,#8285,#8286,#8287,#8288,#8289,#8290,
#8291,#8292,#8293));
#3093=LINE('',#27782,#3843);
#3094=LINE('',#27784,#3844);
#3095=LINE('',#27786,#3845);
#3096=LINE('',#27787,#3846);
#3097=LINE('',#27790,#3847);
#3098=LINE('',#27792,#3848);
#3099=LINE('',#27794,#3849);
#3100=LINE('',#27796,#3850);
#3101=LINE('',#27798,#3851);
#3102=LINE('',#27800,#3852);
#3103=LINE('',#27802,#3853);
#3104=LINE('',#27804,#3854);
#3105=LINE('',#27806,#3855);
#3106=LINE('',#27808,#3856);
#3107=LINE('',#27810,#3857);
#3108=LINE('',#27811,#3858);
#3109=LINE('',#27815,#3859);
#3110=LINE('',#27816,#3860);
#3111=LINE('',#27817,#3861);
#3112=LINE('',#27820,#3862);
#3113=LINE('',#27821,#3863);
#3114=LINE('',#27824,#3864);
#3115=LINE('',#27825,#3865);
#3116=LINE('',#27827,#3866);
#3117=LINE('',#27831,#3867);
#3118=LINE('',#27833,#3868);
#3119=LINE('',#27835,#3869);
#3120=LINE('',#27837,#3870);
#3121=LINE('',#27839,#3871);
#3122=LINE('',#27841,#3872);
#3123=LINE('',#27843,#3873);
#3124=LINE('',#27845,#3874);
#3125=LINE('',#27847,#3875);
#3126=LINE('',#27849,#3876);
#3127=LINE('',#27851,#3877);
#3128=LINE('',#27852,#3878);
#3129=LINE('',#27855,#3879);
#3130=LINE('',#27857,#3880);
#3131=LINE('',#27858,#3881);
#3132=LINE('',#27861,#3882);
#3133=LINE('',#27862,#3883);
#3134=LINE('',#27865,#3884);
#3135=LINE('',#27866,#3885);
#3136=LINE('',#27869,#3886);
#3137=LINE('',#27870,#3887);
#3138=LINE('',#27873,#3888);
#3139=LINE('',#27874,#3889);
#3140=LINE('',#27877,#3890);
#3141=LINE('',#27878,#3891);
#3142=LINE('',#27881,#3892);
#3143=LINE('',#27882,#3893);
#3144=LINE('',#27885,#3894);
#3145=LINE('',#27886,#3895);
#3146=LINE('',#27889,#3896);
#3147=LINE('',#27890,#3897);
#3148=LINE('',#27893,#3898);
#3149=LINE('',#27894,#3899);
#3150=LINE('',#27897,#3900);
#3151=LINE('',#27898,#3901);
#3152=LINE('',#27900,#3902);
#3153=LINE('',#27904,#3903);
#3154=LINE('',#27906,#3904);
#3155=LINE('',#27907,#3905);
#3156=LINE('',#27910,#3906);
#3157=LINE('',#27911,#3907);
#3158=LINE('',#27914,#3908);
#3159=LINE('',#27915,#3909);
#3160=LINE('',#27918,#3910);
#3161=LINE('',#27919,#3911);
#3162=LINE('',#27922,#3912);
#3163=LINE('',#27923,#3913);
#3164=LINE('',#27926,#3914);
#3165=LINE('',#27927,#3915);
#3166=LINE('',#27930,#3916);
#3167=LINE('',#27931,#3917);
#3168=LINE('',#27934,#3918);
#3169=LINE('',#27935,#3919);
#3170=LINE('',#27938,#3920);
#3171=LINE('',#27939,#3921);
#3172=LINE('',#27942,#3922);
#3173=LINE('',#27943,#3923);
#3174=LINE('',#27946,#3924);
#3175=LINE('',#27947,#3925);
#3176=LINE('',#27949,#3926);
#3843=VECTOR('',#12866,1000.);
#3844=VECTOR('',#12867,1000.);
#3845=VECTOR('',#12868,1000.);
#3846=VECTOR('',#12869,1000.);
#3847=VECTOR('',#12870,1000.);
#3848=VECTOR('',#12871,1000.);
#3849=VECTOR('',#12872,1000.);
#3850=VECTOR('',#12873,1000.);
#3851=VECTOR('',#12874,1000.);
#3852=VECTOR('',#12875,1000.);
#3853=VECTOR('',#12876,1000.);
#3854=VECTOR('',#12877,1000.);
#3855=VECTOR('',#12878,1000.);
#3856=VECTOR('',#12879,1000.);
#3857=VECTOR('',#12880,1000.);
#3858=VECTOR('',#12881,1000.);
#3859=VECTOR('',#12884,1000.);
#3860=VECTOR('',#12885,1000.);
#3861=VECTOR('',#12886,1000.);
#3862=VECTOR('',#12889,1000.);
#3863=VECTOR('',#12890,1000.);
#3864=VECTOR('',#12893,1000.);
#3865=VECTOR('',#12894,1000.);
#3866=VECTOR('',#12897,1000.);
#3867=VECTOR('',#12900,1000.);
#3868=VECTOR('',#12901,1000.);
#3869=VECTOR('',#12902,1000.);
#3870=VECTOR('',#12903,1000.);
#3871=VECTOR('',#12904,1000.);
#3872=VECTOR('',#12905,1000.);
#3873=VECTOR('',#12906,1000.);
#3874=VECTOR('',#12907,1000.);
#3875=VECTOR('',#12908,1000.);
#3876=VECTOR('',#12909,1000.);
#3877=VECTOR('',#12910,1000.);
#3878=VECTOR('',#12911,1000.);
#3879=VECTOR('',#12914,1000.);
#3880=VECTOR('',#12915,1000.);
#3881=VECTOR('',#12916,1000.);
#3882=VECTOR('',#12919,1000.);
#3883=VECTOR('',#12920,1000.);
#3884=VECTOR('',#12923,1000.);
#3885=VECTOR('',#12924,1000.);
#3886=VECTOR('',#12927,1000.);
#3887=VECTOR('',#12928,1000.);
#3888=VECTOR('',#12931,1000.);
#3889=VECTOR('',#12932,1000.);
#3890=VECTOR('',#12935,1000.);
#3891=VECTOR('',#12936,1000.);
#3892=VECTOR('',#12939,1000.);
#3893=VECTOR('',#12940,1000.);
#3894=VECTOR('',#12943,1000.);
#3895=VECTOR('',#12944,1000.);
#3896=VECTOR('',#12947,1000.);
#3897=VECTOR('',#12948,1000.);
#3898=VECTOR('',#12951,1000.);
#3899=VECTOR('',#12952,1000.);
#3900=VECTOR('',#12955,1000.);
#3901=VECTOR('',#12956,1000.);
#3902=VECTOR('',#12959,1000.);
#3903=VECTOR('',#12964,1000.);
#3904=VECTOR('',#12965,1000.);
#3905=VECTOR('',#12966,1000.);
#3906=VECTOR('',#12969,1000.);
#3907=VECTOR('',#12970,1000.);
#3908=VECTOR('',#12973,1000.);
#3909=VECTOR('',#12974,1000.);
#3910=VECTOR('',#12977,1000.);
#3911=VECTOR('',#12978,1000.);
#3912=VECTOR('',#12981,1000.);
#3913=VECTOR('',#12982,1000.);
#3914=VECTOR('',#12985,1000.);
#3915=VECTOR('',#12986,1000.);
#3916=VECTOR('',#12989,1000.);
#3917=VECTOR('',#12990,1000.);
#3918=VECTOR('',#12993,1000.);
#3919=VECTOR('',#12994,1000.);
#3920=VECTOR('',#12997,1000.);
#3921=VECTOR('',#12998,1000.);
#3922=VECTOR('',#13001,1000.);
#3923=VECTOR('',#13002,1000.);
#3924=VECTOR('',#13005,1000.);
#3925=VECTOR('',#13006,1000.);
#3926=VECTOR('',#13009,1000.);
#4659=VERTEX_POINT('',#27780);
#4660=VERTEX_POINT('',#27781);
#4661=VERTEX_POINT('',#27783);
#4662=VERTEX_POINT('',#27785);
#4663=VERTEX_POINT('',#27788);
#4664=VERTEX_POINT('',#27789);
#4665=VERTEX_POINT('',#27791);
#4666=VERTEX_POINT('',#27793);
#4667=VERTEX_POINT('',#27795);
#4668=VERTEX_POINT('',#27797);
#4669=VERTEX_POINT('',#27799);
#4670=VERTEX_POINT('',#27801);
#4671=VERTEX_POINT('',#27803);
#4672=VERTEX_POINT('',#27805);
#4673=VERTEX_POINT('',#27807);
#4674=VERTEX_POINT('',#27809);
#4675=VERTEX_POINT('',#27813);
#4676=VERTEX_POINT('',#27814);
#4677=VERTEX_POINT('',#27819);
#4678=VERTEX_POINT('',#27823);
#4679=VERTEX_POINT('',#27829);
#4680=VERTEX_POINT('',#27830);
#4681=VERTEX_POINT('',#27832);
#4682=VERTEX_POINT('',#27834);
#4683=VERTEX_POINT('',#27836);
#4684=VERTEX_POINT('',#27838);
#4685=VERTEX_POINT('',#27840);
#4686=VERTEX_POINT('',#27842);
#4687=VERTEX_POINT('',#27844);
#4688=VERTEX_POINT('',#27846);
#4689=VERTEX_POINT('',#27848);
#4690=VERTEX_POINT('',#27850);
#4691=VERTEX_POINT('',#27854);
#4692=VERTEX_POINT('',#27856);
#4693=VERTEX_POINT('',#27860);
#4694=VERTEX_POINT('',#27864);
#4695=VERTEX_POINT('',#27868);
#4696=VERTEX_POINT('',#27872);
#4697=VERTEX_POINT('',#27876);
#4698=VERTEX_POINT('',#27880);
#4699=VERTEX_POINT('',#27884);
#4700=VERTEX_POINT('',#27888);
#4701=VERTEX_POINT('',#27892);
#4702=VERTEX_POINT('',#27896);
#4703=VERTEX_POINT('',#27903);
#4704=VERTEX_POINT('',#27905);
#4705=VERTEX_POINT('',#27909);
#4706=VERTEX_POINT('',#27913);
#4707=VERTEX_POINT('',#27917);
#4708=VERTEX_POINT('',#27921);
#4709=VERTEX_POINT('',#27925);
#4710=VERTEX_POINT('',#27929);
#4711=VERTEX_POINT('',#27933);
#4712=VERTEX_POINT('',#27937);
#4713=VERTEX_POINT('',#27941);
#4714=VERTEX_POINT('',#27945);
#5876=EDGE_CURVE('',#4659,#4660,#3093,.T.);
#5877=EDGE_CURVE('',#4660,#4661,#3094,.T.);
#5878=EDGE_CURVE('',#4661,#4662,#3095,.T.);
#5879=EDGE_CURVE('',#4662,#4659,#3096,.T.);
#5880=EDGE_CURVE('',#4663,#4664,#3097,.T.);
#5881=EDGE_CURVE('',#4664,#4665,#3098,.T.);
#5882=EDGE_CURVE('',#4665,#4666,#3099,.T.);
#5883=EDGE_CURVE('',#4666,#4667,#3100,.T.);
#5884=EDGE_CURVE('',#4667,#4668,#3101,.T.);
#5885=EDGE_CURVE('',#4668,#4669,#3102,.T.);
#5886=EDGE_CURVE('',#4669,#4670,#3103,.T.);
#5887=EDGE_CURVE('',#4670,#4671,#3104,.T.);
#5888=EDGE_CURVE('',#4671,#4672,#3105,.T.);
#5889=EDGE_CURVE('',#4672,#4673,#3106,.T.);
#5890=EDGE_CURVE('',#4673,#4674,#3107,.T.);
#5891=EDGE_CURVE('',#4674,#4663,#3108,.T.);
#5892=EDGE_CURVE('',#4675,#4676,#3109,.T.);
#5893=EDGE_CURVE('',#4660,#4676,#3110,.T.);
#5894=EDGE_CURVE('',#4659,#4675,#3111,.T.);
#5895=EDGE_CURVE('',#4676,#4677,#3112,.T.);
#5896=EDGE_CURVE('',#4661,#4677,#3113,.T.);
#5897=EDGE_CURVE('',#4677,#4678,#3114,.T.);
#5898=EDGE_CURVE('',#4662,#4678,#3115,.T.);
#5899=EDGE_CURVE('',#4678,#4675,#3116,.T.);
#5900=EDGE_CURVE('',#4679,#4680,#3117,.T.);
#5901=EDGE_CURVE('',#4681,#4679,#3118,.T.);
#5902=EDGE_CURVE('',#4682,#4681,#3119,.T.);
#5903=EDGE_CURVE('',#4683,#4682,#3120,.T.);
#5904=EDGE_CURVE('',#4684,#4683,#3121,.T.);
#5905=EDGE_CURVE('',#4685,#4684,#3122,.T.);
#5906=EDGE_CURVE('',#4686,#4685,#3123,.T.);
#5907=EDGE_CURVE('',#4687,#4686,#3124,.T.);
#5908=EDGE_CURVE('',#4688,#4687,#3125,.T.);
#5909=EDGE_CURVE('',#4689,#4688,#3126,.T.);
#5910=EDGE_CURVE('',#4690,#4689,#3127,.T.);
#5911=EDGE_CURVE('',#4680,#4690,#3128,.T.);
#5912=EDGE_CURVE('',#4691,#4663,#3129,.T.);
#5913=EDGE_CURVE('',#4691,#4692,#3130,.T.);
#5914=EDGE_CURVE('',#4692,#4664,#3131,.T.);
#5915=EDGE_CURVE('',#4692,#4693,#3132,.T.);
#5916=EDGE_CURVE('',#4693,#4665,#3133,.T.);
#5917=EDGE_CURVE('',#4693,#4694,#3134,.T.);
#5918=EDGE_CURVE('',#4694,#4666,#3135,.T.);
#5919=EDGE_CURVE('',#4694,#4695,#3136,.T.);
#5920=EDGE_CURVE('',#4695,#4667,#3137,.T.);
#5921=EDGE_CURVE('',#4695,#4696,#3138,.T.);
#5922=EDGE_CURVE('',#4696,#4668,#3139,.T.);
#5923=EDGE_CURVE('',#4696,#4697,#3140,.T.);
#5924=EDGE_CURVE('',#4697,#4669,#3141,.T.);
#5925=EDGE_CURVE('',#4697,#4698,#3142,.T.);
#5926=EDGE_CURVE('',#4698,#4670,#3143,.T.);
#5927=EDGE_CURVE('',#4698,#4699,#3144,.T.);
#5928=EDGE_CURVE('',#4699,#4671,#3145,.T.);
#5929=EDGE_CURVE('',#4699,#4700,#3146,.T.);
#5930=EDGE_CURVE('',#4700,#4672,#3147,.T.);
#5931=EDGE_CURVE('',#4700,#4701,#3148,.T.);
#5932=EDGE_CURVE('',#4701,#4673,#3149,.T.);
#5933=EDGE_CURVE('',#4701,#4702,#3150,.T.);
#5934=EDGE_CURVE('',#4702,#4674,#3151,.T.);
#5935=EDGE_CURVE('',#4702,#4691,#3152,.T.);
#5936=EDGE_CURVE('',#4703,#4680,#3153,.T.);
#5937=EDGE_CURVE('',#4704,#4703,#3154,.T.);
#5938=EDGE_CURVE('',#4704,#4679,#3155,.T.);
#5939=EDGE_CURVE('',#4705,#4704,#3156,.T.);
#5940=EDGE_CURVE('',#4705,#4681,#3157,.T.);
#5941=EDGE_CURVE('',#4706,#4705,#3158,.T.);
#5942=EDGE_CURVE('',#4706,#4682,#3159,.T.);
#5943=EDGE_CURVE('',#4707,#4706,#3160,.T.);
#5944=EDGE_CURVE('',#4707,#4683,#3161,.T.);
#5945=EDGE_CURVE('',#4708,#4707,#3162,.T.);
#5946=EDGE_CURVE('',#4708,#4684,#3163,.T.);
#5947=EDGE_CURVE('',#4709,#4708,#3164,.T.);
#5948=EDGE_CURVE('',#4709,#4685,#3165,.T.);
#5949=EDGE_CURVE('',#4710,#4709,#3166,.T.);
#5950=EDGE_CURVE('',#4710,#4686,#3167,.T.);
#5951=EDGE_CURVE('',#4711,#4710,#3168,.T.);
#5952=EDGE_CURVE('',#4711,#4687,#3169,.T.);
#5953=EDGE_CURVE('',#4712,#4711,#3170,.T.);
#5954=EDGE_CURVE('',#4712,#4688,#3171,.T.);
#5955=EDGE_CURVE('',#4713,#4712,#3172,.T.);
#5956=EDGE_CURVE('',#4713,#4689,#3173,.T.);
#5957=EDGE_CURVE('',#4714,#4713,#3174,.T.);
#5958=EDGE_CURVE('',#4714,#4690,#3175,.T.);
#5959=EDGE_CURVE('',#4703,#4714,#3176,.T.);
#8126=ORIENTED_EDGE('',*,*,#5876,.T.);
#8127=ORIENTED_EDGE('',*,*,#5877,.T.);
#8128=ORIENTED_EDGE('',*,*,#5878,.T.);
#8129=ORIENTED_EDGE('',*,*,#5879,.T.);
#8130=ORIENTED_EDGE('',*,*,#5880,.T.);
#8131=ORIENTED_EDGE('',*,*,#5881,.T.);
#8132=ORIENTED_EDGE('',*,*,#5882,.T.);
#8133=ORIENTED_EDGE('',*,*,#5883,.T.);
#8134=ORIENTED_EDGE('',*,*,#5884,.T.);
#8135=ORIENTED_EDGE('',*,*,#5885,.T.);
#8136=ORIENTED_EDGE('',*,*,#5886,.T.);
#8137=ORIENTED_EDGE('',*,*,#5887,.T.);
#8138=ORIENTED_EDGE('',*,*,#5888,.T.);
#8139=ORIENTED_EDGE('',*,*,#5889,.T.);
#8140=ORIENTED_EDGE('',*,*,#5890,.T.);
#8141=ORIENTED_EDGE('',*,*,#5891,.T.);
#8142=ORIENTED_EDGE('',*,*,#5892,.T.);
#8143=ORIENTED_EDGE('',*,*,#5893,.F.);
#8144=ORIENTED_EDGE('',*,*,#5876,.F.);
#8145=ORIENTED_EDGE('',*,*,#5894,.T.);
#8146=ORIENTED_EDGE('',*,*,#5895,.T.);
#8147=ORIENTED_EDGE('',*,*,#5896,.F.);
#8148=ORIENTED_EDGE('',*,*,#5877,.F.);
#8149=ORIENTED_EDGE('',*,*,#5893,.T.);
#8150=ORIENTED_EDGE('',*,*,#5897,.T.);
#8151=ORIENTED_EDGE('',*,*,#5898,.F.);
#8152=ORIENTED_EDGE('',*,*,#5878,.F.);
#8153=ORIENTED_EDGE('',*,*,#5896,.T.);
#8154=ORIENTED_EDGE('',*,*,#5899,.T.);
#8155=ORIENTED_EDGE('',*,*,#5894,.F.);
#8156=ORIENTED_EDGE('',*,*,#5879,.F.);
#8157=ORIENTED_EDGE('',*,*,#5898,.T.);
#8158=ORIENTED_EDGE('',*,*,#5892,.F.);
#8159=ORIENTED_EDGE('',*,*,#5899,.F.);
#8160=ORIENTED_EDGE('',*,*,#5897,.F.);
#8161=ORIENTED_EDGE('',*,*,#5895,.F.);
#8162=ORIENTED_EDGE('',*,*,#5900,.F.);
#8163=ORIENTED_EDGE('',*,*,#5901,.F.);
#8164=ORIENTED_EDGE('',*,*,#5902,.F.);
#8165=ORIENTED_EDGE('',*,*,#5903,.F.);
#8166=ORIENTED_EDGE('',*,*,#5904,.F.);
#8167=ORIENTED_EDGE('',*,*,#5905,.F.);
#8168=ORIENTED_EDGE('',*,*,#5906,.F.);
#8169=ORIENTED_EDGE('',*,*,#5907,.F.);
#8170=ORIENTED_EDGE('',*,*,#5908,.F.);
#8171=ORIENTED_EDGE('',*,*,#5909,.F.);
#8172=ORIENTED_EDGE('',*,*,#5910,.F.);
#8173=ORIENTED_EDGE('',*,*,#5911,.F.);
#8174=ORIENTED_EDGE('',*,*,#5880,.F.);
#8175=ORIENTED_EDGE('',*,*,#5912,.F.);
#8176=ORIENTED_EDGE('',*,*,#5913,.T.);
#8177=ORIENTED_EDGE('',*,*,#5914,.T.);
#8178=ORIENTED_EDGE('',*,*,#5881,.F.);
#8179=ORIENTED_EDGE('',*,*,#5914,.F.);
#8180=ORIENTED_EDGE('',*,*,#5915,.T.);
#8181=ORIENTED_EDGE('',*,*,#5916,.T.);
#8182=ORIENTED_EDGE('',*,*,#5882,.F.);
#8183=ORIENTED_EDGE('',*,*,#5916,.F.);
#8184=ORIENTED_EDGE('',*,*,#5917,.T.);
#8185=ORIENTED_EDGE('',*,*,#5918,.T.);
#8186=ORIENTED_EDGE('',*,*,#5883,.F.);
#8187=ORIENTED_EDGE('',*,*,#5918,.F.);
#8188=ORIENTED_EDGE('',*,*,#5919,.T.);
#8189=ORIENTED_EDGE('',*,*,#5920,.T.);
#8190=ORIENTED_EDGE('',*,*,#5884,.F.);
#8191=ORIENTED_EDGE('',*,*,#5920,.F.);
#8192=ORIENTED_EDGE('',*,*,#5921,.T.);
#8193=ORIENTED_EDGE('',*,*,#5922,.T.);
#8194=ORIENTED_EDGE('',*,*,#5885,.F.);
#8195=ORIENTED_EDGE('',*,*,#5922,.F.);
#8196=ORIENTED_EDGE('',*,*,#5923,.T.);
#8197=ORIENTED_EDGE('',*,*,#5924,.T.);
#8198=ORIENTED_EDGE('',*,*,#5886,.F.);
#8199=ORIENTED_EDGE('',*,*,#5924,.F.);
#8200=ORIENTED_EDGE('',*,*,#5925,.T.);
#8201=ORIENTED_EDGE('',*,*,#5926,.T.);
#8202=ORIENTED_EDGE('',*,*,#5887,.F.);
#8203=ORIENTED_EDGE('',*,*,#5926,.F.);
#8204=ORIENTED_EDGE('',*,*,#5927,.T.);
#8205=ORIENTED_EDGE('',*,*,#5928,.T.);
#8206=ORIENTED_EDGE('',*,*,#5888,.F.);
#8207=ORIENTED_EDGE('',*,*,#5928,.F.);
#8208=ORIENTED_EDGE('',*,*,#5929,.T.);
#8209=ORIENTED_EDGE('',*,*,#5930,.T.);
#8210=ORIENTED_EDGE('',*,*,#5889,.F.);
#8211=ORIENTED_EDGE('',*,*,#5930,.F.);
#8212=ORIENTED_EDGE('',*,*,#5931,.T.);
#8213=ORIENTED_EDGE('',*,*,#5932,.T.);
#8214=ORIENTED_EDGE('',*,*,#5890,.F.);
#8215=ORIENTED_EDGE('',*,*,#5932,.F.);
#8216=ORIENTED_EDGE('',*,*,#5933,.T.);
#8217=ORIENTED_EDGE('',*,*,#5934,.T.);
#8218=ORIENTED_EDGE('',*,*,#5891,.F.);
#8219=ORIENTED_EDGE('',*,*,#5934,.F.);
#8220=ORIENTED_EDGE('',*,*,#5935,.T.);
#8221=ORIENTED_EDGE('',*,*,#5912,.T.);
#8222=ORIENTED_EDGE('',*,*,#5913,.F.);
#8223=ORIENTED_EDGE('',*,*,#5935,.F.);
#8224=ORIENTED_EDGE('',*,*,#5933,.F.);
#8225=ORIENTED_EDGE('',*,*,#5931,.F.);
#8226=ORIENTED_EDGE('',*,*,#5929,.F.);
#8227=ORIENTED_EDGE('',*,*,#5927,.F.);
#8228=ORIENTED_EDGE('',*,*,#5925,.F.);
#8229=ORIENTED_EDGE('',*,*,#5923,.F.);
#8230=ORIENTED_EDGE('',*,*,#5921,.F.);
#8231=ORIENTED_EDGE('',*,*,#5919,.F.);
#8232=ORIENTED_EDGE('',*,*,#5917,.F.);
#8233=ORIENTED_EDGE('',*,*,#5915,.F.);
#8234=ORIENTED_EDGE('',*,*,#5900,.T.);
#8235=ORIENTED_EDGE('',*,*,#5936,.F.);
#8236=ORIENTED_EDGE('',*,*,#5937,.F.);
#8237=ORIENTED_EDGE('',*,*,#5938,.T.);
#8238=ORIENTED_EDGE('',*,*,#5901,.T.);
#8239=ORIENTED_EDGE('',*,*,#5938,.F.);
#8240=ORIENTED_EDGE('',*,*,#5939,.F.);
#8241=ORIENTED_EDGE('',*,*,#5940,.T.);
#8242=ORIENTED_EDGE('',*,*,#5902,.T.);
#8243=ORIENTED_EDGE('',*,*,#5940,.F.);
#8244=ORIENTED_EDGE('',*,*,#5941,.F.);
#8245=ORIENTED_EDGE('',*,*,#5942,.T.);
#8246=ORIENTED_EDGE('',*,*,#5903,.T.);
#8247=ORIENTED_EDGE('',*,*,#5942,.F.);
#8248=ORIENTED_EDGE('',*,*,#5943,.F.);
#8249=ORIENTED_EDGE('',*,*,#5944,.T.);
#8250=ORIENTED_EDGE('',*,*,#5904,.T.);
#8251=ORIENTED_EDGE('',*,*,#5944,.F.);
#8252=ORIENTED_EDGE('',*,*,#5945,.F.);
#8253=ORIENTED_EDGE('',*,*,#5946,.T.);
#8254=ORIENTED_EDGE('',*,*,#5905,.T.);
#8255=ORIENTED_EDGE('',*,*,#5946,.F.);
#8256=ORIENTED_EDGE('',*,*,#5947,.F.);
#8257=ORIENTED_EDGE('',*,*,#5948,.T.);
#8258=ORIENTED_EDGE('',*,*,#5906,.T.);
#8259=ORIENTED_EDGE('',*,*,#5948,.F.);
#8260=ORIENTED_EDGE('',*,*,#5949,.F.);
#8261=ORIENTED_EDGE('',*,*,#5950,.T.);
#8262=ORIENTED_EDGE('',*,*,#5907,.T.);
#8263=ORIENTED_EDGE('',*,*,#5950,.F.);
#8264=ORIENTED_EDGE('',*,*,#5951,.F.);
#8265=ORIENTED_EDGE('',*,*,#5952,.T.);
#8266=ORIENTED_EDGE('',*,*,#5908,.T.);
#8267=ORIENTED_EDGE('',*,*,#5952,.F.);
#8268=ORIENTED_EDGE('',*,*,#5953,.F.);
#8269=ORIENTED_EDGE('',*,*,#5954,.T.);
#8270=ORIENTED_EDGE('',*,*,#5909,.T.);
#8271=ORIENTED_EDGE('',*,*,#5954,.F.);
#8272=ORIENTED_EDGE('',*,*,#5955,.F.);
#8273=ORIENTED_EDGE('',*,*,#5956,.T.);
#8274=ORIENTED_EDGE('',*,*,#5910,.T.);
#8275=ORIENTED_EDGE('',*,*,#5956,.F.);
#8276=ORIENTED_EDGE('',*,*,#5957,.F.);
#8277=ORIENTED_EDGE('',*,*,#5958,.T.);
#8278=ORIENTED_EDGE('',*,*,#5911,.T.);
#8279=ORIENTED_EDGE('',*,*,#5958,.F.);
#8280=ORIENTED_EDGE('',*,*,#5959,.F.);
#8281=ORIENTED_EDGE('',*,*,#5936,.T.);
#8282=ORIENTED_EDGE('',*,*,#5937,.T.);
#8283=ORIENTED_EDGE('',*,*,#5959,.T.);
#8284=ORIENTED_EDGE('',*,*,#5957,.T.);
#8285=ORIENTED_EDGE('',*,*,#5955,.T.);
#8286=ORIENTED_EDGE('',*,*,#5953,.T.);
#8287=ORIENTED_EDGE('',*,*,#5951,.T.);
#8288=ORIENTED_EDGE('',*,*,#5949,.T.);
#8289=ORIENTED_EDGE('',*,*,#5947,.T.);
#8290=ORIENTED_EDGE('',*,*,#5945,.T.);
#8291=ORIENTED_EDGE('',*,*,#5943,.T.);
#8292=ORIENTED_EDGE('',*,*,#5941,.T.);
#8293=ORIENTED_EDGE('',*,*,#5939,.T.);
#9724=ADVANCED_FACE('',(#1358,#520),#926,.F.);
#9725=ADVANCED_FACE('',(#1359),#927,.F.);
#9726=ADVANCED_FACE('',(#1360),#928,.F.);
#9727=ADVANCED_FACE('',(#1361),#929,.F.);
#9728=ADVANCED_FACE('',(#1362),#930,.F.);
#9729=ADVANCED_FACE('',(#1363,#521),#931,.T.);
#9730=ADVANCED_FACE('',(#1364),#932,.T.);
#9731=ADVANCED_FACE('',(#1365),#933,.T.);
#9732=ADVANCED_FACE('',(#1366),#934,.T.);
#9733=ADVANCED_FACE('',(#1367),#935,.T.);
#9734=ADVANCED_FACE('',(#1368),#936,.T.);
#9735=ADVANCED_FACE('',(#1369),#937,.T.);
#9736=ADVANCED_FACE('',(#1370),#938,.T.);
#9737=ADVANCED_FACE('',(#1371),#939,.T.);
#9738=ADVANCED_FACE('',(#1372),#940,.T.);
#9739=ADVANCED_FACE('',(#1373),#941,.T.);
#9740=ADVANCED_FACE('',(#1374),#942,.T.);
#9741=ADVANCED_FACE('',(#1375),#943,.T.);
#9742=ADVANCED_FACE('',(#1376),#944,.F.);
#9743=ADVANCED_FACE('',(#1377),#945,.F.);
#9744=ADVANCED_FACE('',(#1378),#946,.F.);
#9745=ADVANCED_FACE('',(#1379),#947,.F.);
#9746=ADVANCED_FACE('',(#1380),#948,.F.);
#9747=ADVANCED_FACE('',(#1381),#949,.F.);
#9748=ADVANCED_FACE('',(#1382),#950,.F.);
#9749=ADVANCED_FACE('',(#1383),#951,.F.);
#9750=ADVANCED_FACE('',(#1384),#952,.F.);
#9751=ADVANCED_FACE('',(#1385),#953,.F.);
#9752=ADVANCED_FACE('',(#1386),#954,.F.);
#9753=ADVANCED_FACE('',(#1387),#955,.F.);
#9754=ADVANCED_FACE('',(#1388),#956,.F.);
#9755=ADVANCED_FACE('',(#1389),#957,.F.);
#9956=CLOSED_SHELL('',(#9724,#9725,#9726,#9727,#9728,#9729,#9730,#9731,
#9732,#9733,#9734,#9735,#9736,#9737,#9738,#9739,#9740,#9741,#9742,#9743,
#9744,#9745,#9746,#9747,#9748,#9749,#9750,#9751,#9752,#9753,#9754,#9755));
#10835=AXIS2_PLACEMENT_3D('',#27778,#12862,#12863);
#10836=AXIS2_PLACEMENT_3D('',#27779,#12864,#12865);
#10837=AXIS2_PLACEMENT_3D('',#27812,#12882,#12883);
#10838=AXIS2_PLACEMENT_3D('',#27818,#12887,#12888);
#10839=AXIS2_PLACEMENT_3D('',#27822,#12891,#12892);
#10840=AXIS2_PLACEMENT_3D('',#27826,#12895,#12896);
#10841=AXIS2_PLACEMENT_3D('',#27828,#12898,#12899);
#10842=AXIS2_PLACEMENT_3D('',#27853,#12912,#12913);
#10843=AXIS2_PLACEMENT_3D('',#27859,#12917,#12918);
#10844=AXIS2_PLACEMENT_3D('',#27863,#12921,#12922);
#10845=AXIS2_PLACEMENT_3D('',#27867,#12925,#12926);
#10846=AXIS2_PLACEMENT_3D('',#27871,#12929,#12930);
#10847=AXIS2_PLACEMENT_3D('',#27875,#12933,#12934);
#10848=AXIS2_PLACEMENT_3D('',#27879,#12937,#12938);
#10849=AXIS2_PLACEMENT_3D('',#27883,#12941,#12942);
#10850=AXIS2_PLACEMENT_3D('',#27887,#12945,#12946);
#10851=AXIS2_PLACEMENT_3D('',#27891,#12949,#12950);
#10852=AXIS2_PLACEMENT_3D('',#27895,#12953,#12954);
#10853=AXIS2_PLACEMENT_3D('',#27899,#12957,#12958);
#10854=AXIS2_PLACEMENT_3D('',#27901,#12960,#12961);
#10855=AXIS2_PLACEMENT_3D('',#27902,#12962,#12963);
#10856=AXIS2_PLACEMENT_3D('',#27908,#12967,#12968);
#10857=AXIS2_PLACEMENT_3D('',#27912,#12971,#12972);
#10858=AXIS2_PLACEMENT_3D('',#27916,#12975,#12976);
#10859=AXIS2_PLACEMENT_3D('',#27920,#12979,#12980);
#10860=AXIS2_PLACEMENT_3D('',#27924,#12983,#12984);
#10861=AXIS2_PLACEMENT_3D('',#27928,#12987,#12988);
#10862=AXIS2_PLACEMENT_3D('',#27932,#12991,#12992);
#10863=AXIS2_PLACEMENT_3D('',#27936,#12995,#12996);
#10864=AXIS2_PLACEMENT_3D('',#27940,#12999,#13000);
#10865=AXIS2_PLACEMENT_3D('',#27944,#13003,#13004);
#10866=AXIS2_PLACEMENT_3D('',#27948,#13007,#13008);
#10867=AXIS2_PLACEMENT_3D('',#27950,#13010,#13011);
#12862=DIRECTION('axis',(0.,0.,1.));
#12863=DIRECTION('refdir',(1.,0.,0.));
#12864=DIRECTION('center_axis',(0.,-1.,0.));
#12865=DIRECTION('ref_axis',(0.,0.,-1.));
#12866=DIRECTION('',(0.,0.,-1.));
#12867=DIRECTION('',(-1.,0.,0.));
#12868=DIRECTION('',(0.,0.,1.));
#12869=DIRECTION('',(1.,0.,0.));
#12870=DIRECTION('',(0.,0.,-1.));
#12871=DIRECTION('',(1.,0.,0.));
#12872=DIRECTION('',(0.,0.,1.));
#12873=DIRECTION('',(1.,0.,0.));
#12874=DIRECTION('',(0.,0.,-1.));
#12875=DIRECTION('',(1.,0.,0.));
#12876=DIRECTION('',(0.,0.,1.));
#12877=DIRECTION('',(-1.,0.,0.));
#12878=DIRECTION('',(0.,0.,-1.));
#12879=DIRECTION('',(-1.,0.,0.));
#12880=DIRECTION('',(0.,0.,1.));
#12881=DIRECTION('',(-1.,0.,0.));
#12882=DIRECTION('center_axis',(-1.,0.,0.));
#12883=DIRECTION('ref_axis',(0.,0.,1.));
#12884=DIRECTION('',(0.,0.,-1.));
#12885=DIRECTION('',(0.,-1.,0.));
#12886=DIRECTION('',(0.,-1.,0.));
#12887=DIRECTION('center_axis',(0.,0.,1.));
#12888=DIRECTION('ref_axis',(1.,0.,0.));
#12889=DIRECTION('',(-1.,0.,0.));
#12890=DIRECTION('',(0.,-1.,0.));
#12891=DIRECTION('center_axis',(1.,0.,0.));
#12892=DIRECTION('ref_axis',(0.,0.,-1.));
#12893=DIRECTION('',(0.,0.,1.));
#12894=DIRECTION('',(0.,-1.,0.));
#12895=DIRECTION('center_axis',(0.,0.,-1.));
#12896=DIRECTION('ref_axis',(-1.,0.,0.));
#12897=DIRECTION('',(1.,0.,0.));
#12898=DIRECTION('center_axis',(0.,-1.,0.));
#12899=DIRECTION('ref_axis',(0.,0.,-1.));
#12900=DIRECTION('',(0.,0.,-1.));
#12901=DIRECTION('',(-1.,0.,0.));
#12902=DIRECTION('',(0.,0.,1.));
#12903=DIRECTION('',(-1.,0.,0.));
#12904=DIRECTION('',(0.,0.,-1.));
#12905=DIRECTION('',(-1.,0.,0.));
#12906=DIRECTION('',(0.,0.,1.));
#12907=DIRECTION('',(1.,0.,0.));
#12908=DIRECTION('',(0.,0.,-1.));
#12909=DIRECTION('',(1.,0.,0.));
#12910=DIRECTION('',(0.,0.,1.));
#12911=DIRECTION('',(1.,0.,0.));
#12912=DIRECTION('center_axis',(1.,0.,0.));
#12913=DIRECTION('ref_axis',(0.,0.,-1.));
#12914=DIRECTION('',(0.,1.,0.));
#12915=DIRECTION('',(0.,0.,-1.));
#12916=DIRECTION('',(0.,1.,0.));
#12917=DIRECTION('center_axis',(0.,0.,1.));
#12918=DIRECTION('ref_axis',(1.,0.,0.));
#12919=DIRECTION('',(1.,0.,0.));
#12920=DIRECTION('',(0.,1.,0.));
#12921=DIRECTION('center_axis',(-1.,0.,0.));
#12922=DIRECTION('ref_axis',(0.,0.,1.));
#12923=DIRECTION('',(0.,0.,1.));
#12924=DIRECTION('',(0.,1.,0.));
#12925=DIRECTION('center_axis',(0.,0.,1.));
#12926=DIRECTION('ref_axis',(1.,0.,0.));
#12927=DIRECTION('',(1.,0.,0.));
#12928=DIRECTION('',(0.,1.,0.));
#12929=DIRECTION('center_axis',(1.,0.,0.));
#12930=DIRECTION('ref_axis',(0.,0.,-1.));
#12931=DIRECTION('',(0.,0.,-1.));
#12932=DIRECTION('',(0.,1.,0.));
#12933=DIRECTION('center_axis',(0.,0.,1.));
#12934=DIRECTION('ref_axis',(1.,0.,0.));
#12935=DIRECTION('',(1.,0.,0.));
#12936=DIRECTION('',(0.,1.,0.));
#12937=DIRECTION('center_axis',(-1.,0.,0.));
#12938=DIRECTION('ref_axis',(0.,0.,1.));
#12939=DIRECTION('',(0.,0.,1.));
#12940=DIRECTION('',(0.,1.,0.));
#12941=DIRECTION('center_axis',(0.,0.,-1.));
#12942=DIRECTION('ref_axis',(-1.,0.,0.));
#12943=DIRECTION('',(-1.,0.,0.));
#12944=DIRECTION('',(0.,1.,0.));
#12945=DIRECTION('center_axis',(1.,0.,0.));
#12946=DIRECTION('ref_axis',(0.,0.,-1.));
#12947=DIRECTION('',(0.,0.,-1.));
#12948=DIRECTION('',(0.,1.,0.));
#12949=DIRECTION('center_axis',(0.,0.,-1.));
#12950=DIRECTION('ref_axis',(-1.,0.,0.));
#12951=DIRECTION('',(-1.,0.,0.));
#12952=DIRECTION('',(0.,1.,0.));
#12953=DIRECTION('center_axis',(-1.,0.,0.));
#12954=DIRECTION('ref_axis',(0.,0.,1.));
#12955=DIRECTION('',(0.,0.,1.));
#12956=DIRECTION('',(0.,1.,0.));
#12957=DIRECTION('center_axis',(0.,0.,-1.));
#12958=DIRECTION('ref_axis',(-1.,0.,0.));
#12959=DIRECTION('',(-1.,0.,0.));
#12960=DIRECTION('center_axis',(0.,-1.,0.));
#12961=DIRECTION('ref_axis',(0.,0.,-1.));
#12962=DIRECTION('center_axis',(-1.,0.,0.));
#12963=DIRECTION('ref_axis',(0.,0.,1.));
#12964=DIRECTION('',(0.,-1.,0.));
#12965=DIRECTION('',(0.,0.,-1.));
#12966=DIRECTION('',(0.,-1.,0.));
#12967=DIRECTION('center_axis',(0.,0.,1.));
#12968=DIRECTION('ref_axis',(1.,0.,0.));
#12969=DIRECTION('',(-1.,0.,0.));
#12970=DIRECTION('',(0.,-1.,0.));
#12971=DIRECTION('center_axis',(1.,0.,0.));
#12972=DIRECTION('ref_axis',(0.,0.,-1.));
#12973=DIRECTION('',(0.,0.,1.));
#12974=DIRECTION('',(0.,-1.,0.));
#12975=DIRECTION('center_axis',(0.,0.,1.));
#12976=DIRECTION('ref_axis',(1.,0.,0.));
#12977=DIRECTION('',(-1.,0.,0.));
#12978=DIRECTION('',(0.,-1.,0.));
#12979=DIRECTION('center_axis',(-1.,0.,0.));
#12980=DIRECTION('ref_axis',(0.,0.,1.));
#12981=DIRECTION('',(0.,0.,-1.));
#12982=DIRECTION('',(0.,-1.,0.));
#12983=DIRECTION('center_axis',(0.,0.,1.));
#12984=DIRECTION('ref_axis',(1.,0.,0.));
#12985=DIRECTION('',(-1.,0.,0.));
#12986=DIRECTION('',(0.,-1.,0.));
#12987=DIRECTION('center_axis',(1.,0.,0.));
#12988=DIRECTION('ref_axis',(0.,0.,-1.));
#12989=DIRECTION('',(0.,0.,1.));
#12990=DIRECTION('',(0.,-1.,0.));
#12991=DIRECTION('center_axis',(0.,0.,-1.));
#12992=DIRECTION('ref_axis',(-1.,0.,0.));
#12993=DIRECTION('',(1.,0.,0.));
#12994=DIRECTION('',(0.,-1.,0.));
#12995=DIRECTION('center_axis',(-1.,0.,0.));
#12996=DIRECTION('ref_axis',(0.,0.,1.));
#12997=DIRECTION('',(0.,0.,-1.));
#12998=DIRECTION('',(0.,-1.,0.));
#12999=DIRECTION('center_axis',(0.,0.,-1.));
#13000=DIRECTION('ref_axis',(-1.,0.,0.));
#13001=DIRECTION('',(1.,0.,0.));
#13002=DIRECTION('',(0.,-1.,0.));
#13003=DIRECTION('center_axis',(1.,0.,0.));
#13004=DIRECTION('ref_axis',(0.,0.,-1.));
#13005=DIRECTION('',(0.,0.,1.));
#13006=DIRECTION('',(0.,-1.,0.));
#13007=DIRECTION('center_axis',(0.,0.,-1.));
#13008=DIRECTION('ref_axis',(-1.,0.,0.));
#13009=DIRECTION('',(1.,0.,0.));
#13010=DIRECTION('center_axis',(0.,1.,0.));
#13011=DIRECTION('ref_axis',(0.,0.,-1.));
#27778=CARTESIAN_POINT('',(0.,0.,0.));
#27779=CARTESIAN_POINT('Origin',(0.,7.5,0.));
#27780=CARTESIAN_POINT('',(3.5,7.5,3.75));
#27781=CARTESIAN_POINT('',(3.5,7.5,-3.75));
#27782=CARTESIAN_POINT('',(3.5,7.5,3.75));
#27783=CARTESIAN_POINT('',(-3.5,7.5,-3.75));
#27784=CARTESIAN_POINT('',(-3.5,7.5,-3.75));
#27785=CARTESIAN_POINT('',(-3.5,7.5,3.75));
#27786=CARTESIAN_POINT('',(-3.5,7.5,3.75));
#27787=CARTESIAN_POINT('',(-3.5,7.5,3.75));
#27788=CARTESIAN_POINT('',(-1.13411058466707,7.5,1.43083506494736));
#27789=CARTESIAN_POINT('',(-1.13411058466707,7.5,-2.06916493505264));
#27790=CARTESIAN_POINT('',(-1.13411058466707,7.5,1.43083506494736));
#27791=CARTESIAN_POINT('',(-0.820008020564509,7.5,-2.06916493505264));
#27792=CARTESIAN_POINT('',(-1.13411058466707,7.5,-2.06916493505264));
#27793=CARTESIAN_POINT('',(-0.820008020564509,7.5,-0.633267499155203));
#27794=CARTESIAN_POINT('',(-0.820008020564509,7.5,-2.06916493505264));
#27795=CARTESIAN_POINT('',(0.974863774307286,7.5,-0.633267499155203));
#27796=CARTESIAN_POINT('',(-0.820008020564509,7.5,-0.633267499155203));
#27797=CARTESIAN_POINT('',(0.974863774307286,7.5,-2.06916493505264));
#27798=CARTESIAN_POINT('',(0.974863774307286,7.5,-0.633267499155203));
#27799=CARTESIAN_POINT('',(1.28896633840985,7.5,-2.06916493505264));
#27800=CARTESIAN_POINT('',(0.974863774307286,7.5,-2.06916493505264));
#27801=CARTESIAN_POINT('',(1.28896633840985,7.5,1.43083506494736));
#27802=CARTESIAN_POINT('',(1.28896633840985,7.5,-2.06916493505264));
#27803=CARTESIAN_POINT('',(0.974863774307286,7.5,1.43083506494736));
#27804=CARTESIAN_POINT('',(1.28896633840985,7.5,1.43083506494736));
#27805=CARTESIAN_POINT('',(0.974863774307286,7.5,-0.274293140180844));
#27806=CARTESIAN_POINT('',(0.974863774307286,7.5,1.43083506494736));
#27807=CARTESIAN_POINT('',(-0.820008020564509,7.5,-0.274293140180844));
#27808=CARTESIAN_POINT('',(0.974863774307286,7.5,-0.274293140180844));
#27809=CARTESIAN_POINT('',(-0.820008020564509,7.5,1.43083506494736));
#27810=CARTESIAN_POINT('',(-0.820008020564509,7.5,-0.274293140180844));
#27811=CARTESIAN_POINT('',(-0.820008020564509,7.5,1.43083506494736));
#27812=CARTESIAN_POINT('Origin',(3.5,7.5,3.75));
#27813=CARTESIAN_POINT('',(3.5,0.,3.75));
#27814=CARTESIAN_POINT('',(3.5,0.,-3.75));
#27815=CARTESIAN_POINT('',(3.5,0.,3.75));
#27816=CARTESIAN_POINT('',(3.5,7.5,-3.75));
#27817=CARTESIAN_POINT('',(3.5,7.5,3.75));
#27818=CARTESIAN_POINT('Origin',(-3.5,7.5,-3.75));
#27819=CARTESIAN_POINT('',(-3.5,0.,-3.75));
#27820=CARTESIAN_POINT('',(-3.5,0.,-3.75));
#27821=CARTESIAN_POINT('',(-3.5,7.5,-3.75));
#27822=CARTESIAN_POINT('Origin',(-3.5,7.5,3.75));
#27823=CARTESIAN_POINT('',(-3.5,0.,3.75));
#27824=CARTESIAN_POINT('',(-3.5,0.,3.75));
#27825=CARTESIAN_POINT('',(-3.5,7.5,3.75));
#27826=CARTESIAN_POINT('Origin',(-3.5,7.5,3.75));
#27827=CARTESIAN_POINT('',(-3.5,0.,3.75));
#27828=CARTESIAN_POINT('Origin',(0.,0.,0.));
#27829=CARTESIAN_POINT('',(-1.13411058466707,0.,1.43083506494736));
#27830=CARTESIAN_POINT('',(-1.13411058466707,0.,-2.06916493505264));
#27831=CARTESIAN_POINT('',(-1.13411058466707,0.,1.43083506494736));
#27832=CARTESIAN_POINT('',(-0.820008020564509,0.,1.43083506494736));
#27833=CARTESIAN_POINT('',(-0.820008020564509,0.,1.43083506494736));
#27834=CARTESIAN_POINT('',(-0.820008020564509,0.,-0.274293140180844));
#27835=CARTESIAN_POINT('',(-0.820008020564509,0.,-0.274293140180844));
#27836=CARTESIAN_POINT('',(0.974863774307286,0.,-0.274293140180844));
#27837=CARTESIAN_POINT('',(0.974863774307286,0.,-0.274293140180844));
#27838=CARTESIAN_POINT('',(0.974863774307286,0.,1.43083506494736));
#27839=CARTESIAN_POINT('',(0.974863774307286,0.,1.43083506494736));
#27840=CARTESIAN_POINT('',(1.28896633840985,0.,1.43083506494736));
#27841=CARTESIAN_POINT('',(1.28896633840985,0.,1.43083506494736));
#27842=CARTESIAN_POINT('',(1.28896633840985,0.,-2.06916493505264));
#27843=CARTESIAN_POINT('',(1.28896633840985,0.,-2.06916493505264));
#27844=CARTESIAN_POINT('',(0.974863774307286,0.,-2.06916493505264));
#27845=CARTESIAN_POINT('',(0.974863774307286,0.,-2.06916493505264));
#27846=CARTESIAN_POINT('',(0.974863774307286,0.,-0.633267499155203));
#27847=CARTESIAN_POINT('',(0.974863774307286,0.,-0.633267499155203));
#27848=CARTESIAN_POINT('',(-0.820008020564509,0.,-0.633267499155203));
#27849=CARTESIAN_POINT('',(-0.820008020564509,0.,-0.633267499155203));
#27850=CARTESIAN_POINT('',(-0.820008020564509,0.,-2.06916493505264));
#27851=CARTESIAN_POINT('',(-0.820008020564509,0.,-2.06916493505264));
#27852=CARTESIAN_POINT('',(-1.13411058466707,0.,-2.06916493505264));
#27853=CARTESIAN_POINT('Origin',(-1.13411058466707,7.45,1.43083506494736));
#27854=CARTESIAN_POINT('',(-1.13411058466707,7.45,1.43083506494736));
#27855=CARTESIAN_POINT('',(-1.13411058466707,7.45,1.43083506494736));
#27856=CARTESIAN_POINT('',(-1.13411058466707,7.45,-2.06916493505264));
#27857=CARTESIAN_POINT('',(-1.13411058466707,7.45,1.43083506494736));
#27858=CARTESIAN_POINT('',(-1.13411058466707,7.45,-2.06916493505264));
#27859=CARTESIAN_POINT('Origin',(-1.13411058466707,7.45,-2.06916493505264));
#27860=CARTESIAN_POINT('',(-0.820008020564509,7.45,-2.06916493505264));
#27861=CARTESIAN_POINT('',(-1.13411058466707,7.45,-2.06916493505264));
#27862=CARTESIAN_POINT('',(-0.820008020564509,7.45,-2.06916493505264));
#27863=CARTESIAN_POINT('Origin',(-0.820008020564509,7.45,-2.06916493505264));
#27864=CARTESIAN_POINT('',(-0.820008020564509,7.45,-0.633267499155203));
#27865=CARTESIAN_POINT('',(-0.820008020564509,7.45,-2.06916493505264));
#27866=CARTESIAN_POINT('',(-0.820008020564509,7.45,-0.633267499155203));
#27867=CARTESIAN_POINT('Origin',(-0.820008020564509,7.45,-0.633267499155203));
#27868=CARTESIAN_POINT('',(0.974863774307286,7.45,-0.633267499155203));
#27869=CARTESIAN_POINT('',(-0.820008020564509,7.45,-0.633267499155203));
#27870=CARTESIAN_POINT('',(0.974863774307286,7.45,-0.633267499155203));
#27871=CARTESIAN_POINT('Origin',(0.974863774307286,7.45,-0.633267499155203));
#27872=CARTESIAN_POINT('',(0.974863774307286,7.45,-2.06916493505264));
#27873=CARTESIAN_POINT('',(0.974863774307286,7.45,-0.633267499155203));
#27874=CARTESIAN_POINT('',(0.974863774307286,7.45,-2.06916493505264));
#27875=CARTESIAN_POINT('Origin',(0.974863774307286,7.45,-2.06916493505264));
#27876=CARTESIAN_POINT('',(1.28896633840985,7.45,-2.06916493505264));
#27877=CARTESIAN_POINT('',(0.974863774307286,7.45,-2.06916493505264));
#27878=CARTESIAN_POINT('',(1.28896633840985,7.45,-2.06916493505264));
#27879=CARTESIAN_POINT('Origin',(1.28896633840985,7.45,-2.06916493505264));
#27880=CARTESIAN_POINT('',(1.28896633840985,7.45,1.43083506494736));
#27881=CARTESIAN_POINT('',(1.28896633840985,7.45,-2.06916493505264));
#27882=CARTESIAN_POINT('',(1.28896633840985,7.45,1.43083506494736));
#27883=CARTESIAN_POINT('Origin',(1.28896633840985,7.45,1.43083506494736));
#27884=CARTESIAN_POINT('',(0.974863774307286,7.45,1.43083506494736));
#27885=CARTESIAN_POINT('',(1.28896633840985,7.45,1.43083506494736));
#27886=CARTESIAN_POINT('',(0.974863774307286,7.45,1.43083506494736));
#27887=CARTESIAN_POINT('Origin',(0.974863774307286,7.45,1.43083506494736));
#27888=CARTESIAN_POINT('',(0.974863774307286,7.45,-0.274293140180844));
#27889=CARTESIAN_POINT('',(0.974863774307286,7.45,1.43083506494736));
#27890=CARTESIAN_POINT('',(0.974863774307286,7.45,-0.274293140180844));
#27891=CARTESIAN_POINT('Origin',(0.974863774307286,7.45,-0.274293140180844));
#27892=CARTESIAN_POINT('',(-0.820008020564509,7.45,-0.274293140180844));
#27893=CARTESIAN_POINT('',(0.974863774307286,7.45,-0.274293140180844));
#27894=CARTESIAN_POINT('',(-0.820008020564509,7.45,-0.274293140180844));
#27895=CARTESIAN_POINT('Origin',(-0.820008020564509,7.45,-0.274293140180844));
#27896=CARTESIAN_POINT('',(-0.820008020564509,7.45,1.43083506494736));
#27897=CARTESIAN_POINT('',(-0.820008020564509,7.45,-0.274293140180844));
#27898=CARTESIAN_POINT('',(-0.820008020564509,7.45,1.43083506494736));
#27899=CARTESIAN_POINT('Origin',(-0.820008020564509,7.45,1.43083506494736));
#27900=CARTESIAN_POINT('',(-0.820008020564509,7.45,1.43083506494736));
#27901=CARTESIAN_POINT('Origin',(0.,7.45,0.));
#27902=CARTESIAN_POINT('Origin',(-1.13411058466707,0.05,1.43083506494736));
#27903=CARTESIAN_POINT('',(-1.13411058466707,0.05,-2.06916493505264));
#27904=CARTESIAN_POINT('',(-1.13411058466707,0.05,-2.06916493505264));
#27905=CARTESIAN_POINT('',(-1.13411058466707,0.05,1.43083506494736));
#27906=CARTESIAN_POINT('',(-1.13411058466707,0.05,1.43083506494736));
#27907=CARTESIAN_POINT('',(-1.13411058466707,0.05,1.43083506494736));
#27908=CARTESIAN_POINT('Origin',(-0.820008020564509,0.05,1.43083506494736));
#27909=CARTESIAN_POINT('',(-0.820008020564509,0.05,1.43083506494736));
#27910=CARTESIAN_POINT('',(-0.820008020564509,0.05,1.43083506494736));
#27911=CARTESIAN_POINT('',(-0.820008020564509,0.05,1.43083506494736));
#27912=CARTESIAN_POINT('Origin',(-0.820008020564509,0.05,-0.274293140180844));
#27913=CARTESIAN_POINT('',(-0.820008020564509,0.05,-0.274293140180844));
#27914=CARTESIAN_POINT('',(-0.820008020564509,0.05,-0.274293140180844));
#27915=CARTESIAN_POINT('',(-0.820008020564509,0.05,-0.274293140180844));
#27916=CARTESIAN_POINT('Origin',(0.974863774307286,0.05,-0.274293140180844));
#27917=CARTESIAN_POINT('',(0.974863774307286,0.05,-0.274293140180844));
#27918=CARTESIAN_POINT('',(0.974863774307286,0.05,-0.274293140180844));
#27919=CARTESIAN_POINT('',(0.974863774307286,0.05,-0.274293140180844));
#27920=CARTESIAN_POINT('Origin',(0.974863774307286,0.05,1.43083506494736));
#27921=CARTESIAN_POINT('',(0.974863774307286,0.05,1.43083506494736));
#27922=CARTESIAN_POINT('',(0.974863774307286,0.05,1.43083506494736));
#27923=CARTESIAN_POINT('',(0.974863774307286,0.05,1.43083506494736));
#27924=CARTESIAN_POINT('Origin',(1.28896633840985,0.05,1.43083506494736));
#27925=CARTESIAN_POINT('',(1.28896633840985,0.05,1.43083506494736));
#27926=CARTESIAN_POINT('',(1.28896633840985,0.05,1.43083506494736));
#27927=CARTESIAN_POINT('',(1.28896633840985,0.05,1.43083506494736));
#27928=CARTESIAN_POINT('Origin',(1.28896633840985,0.05,-2.06916493505264));
#27929=CARTESIAN_POINT('',(1.28896633840985,0.05,-2.06916493505264));
#27930=CARTESIAN_POINT('',(1.28896633840985,0.05,-2.06916493505264));
#27931=CARTESIAN_POINT('',(1.28896633840985,0.05,-2.06916493505264));
#27932=CARTESIAN_POINT('Origin',(0.974863774307286,0.05,-2.06916493505264));
#27933=CARTESIAN_POINT('',(0.974863774307286,0.05,-2.06916493505264));
#27934=CARTESIAN_POINT('',(0.974863774307286,0.05,-2.06916493505264));
#27935=CARTESIAN_POINT('',(0.974863774307286,0.05,-2.06916493505264));
#27936=CARTESIAN_POINT('Origin',(0.974863774307286,0.05,-0.633267499155203));
#27937=CARTESIAN_POINT('',(0.974863774307286,0.05,-0.633267499155203));
#27938=CARTESIAN_POINT('',(0.974863774307286,0.05,-0.633267499155203));
#27939=CARTESIAN_POINT('',(0.974863774307286,0.05,-0.633267499155203));
#27940=CARTESIAN_POINT('Origin',(-0.820008020564509,0.05,-0.633267499155203));
#27941=CARTESIAN_POINT('',(-0.820008020564509,0.05,-0.633267499155203));
#27942=CARTESIAN_POINT('',(-0.820008020564509,0.05,-0.633267499155203));
#27943=CARTESIAN_POINT('',(-0.820008020564509,0.05,-0.633267499155203));
#27944=CARTESIAN_POINT('Origin',(-0.820008020564509,0.05,-2.06916493505264));
#27945=CARTESIAN_POINT('',(-0.820008020564509,0.05,-2.06916493505264));
#27946=CARTESIAN_POINT('',(-0.820008020564509,0.05,-2.06916493505264));
#27947=CARTESIAN_POINT('',(-0.820008020564509,0.05,-2.06916493505264));
#27948=CARTESIAN_POINT('Origin',(-1.13411058466707,0.05,-2.06916493505264));
#27949=CARTESIAN_POINT('',(-1.13411058466707,0.05,-2.06916493505264));
#27950=CARTESIAN_POINT('Origin',(0.,0.05,0.));
#32970=UNCERTAINTY_MEASURE_WITH_UNIT(LENGTH_MEASURE(0.01),#33017,
'DISTANCE_ACCURACY_VALUE',
'Maximum model space distance between geometric entities at asserted c
onnectivities');
#32984=UNCERTAINTY_MEASURE_WITH_UNIT(LENGTH_MEASURE(0.01),#33017,
'DISTANCE_ACCURACY_VALUE',
'Maximum model space distance between geometric entities at asserted c
onnectivities');
#33002=(
GEOMETRIC_REPRESENTATION_CONTEXT(3)
GLOBAL_UNCERTAINTY_ASSIGNED_CONTEXT((#32970))
GLOBAL_UNIT_ASSIGNED_CONTEXT((#33017,#33019,#33020))
REPRESENTATION_CONTEXT('','3D')
);
#33016=(
GEOMETRIC_REPRESENTATION_CONTEXT(3)
GLOBAL_UNCERTAINTY_ASSIGNED_CONTEXT((#32984))
GLOBAL_UNIT_ASSIGNED_CONTEXT((#33017,#33019,#33020))
REPRESENTATION_CONTEXT('','3D')
);
#33017=(
LENGTH_UNIT()
NAMED_UNIT(*)
SI_UNIT(.MILLI.,.METRE.)
);
#33019=(
NAMED_UNIT(*)
PLANE_ANGLE_UNIT()
SI_UNIT($,.RADIAN.)
);
#33020=(
NAMED_UNIT(*)
SI_UNIT($,.STERADIAN.)
SOLID_ANGLE_UNIT()
);
#33038=SHAPE_DEFINITION_REPRESENTATION(#33077,#33141);
#33077=PRODUCT_DEFINITION_SHAPE('',$,#33173);
#33141=SHAPE_REPRESENTATION('',(#10835),#33002);
#33155=PRODUCT_DEFINITION_CONTEXT('part definition',#33250,'design');
#33173=PRODUCT_DEFINITION(
'P_Torque Wrench_Pivot Cube_PRT-TQ-1012-07_M_Rev00','PRT-TQ-1012-07',#33204,
#33155);
#33204=PRODUCT_DEFINITION_FORMATION('',$,#33269);
#33250=APPLICATION_CONTEXT(
'Core Data for Automotive Mechanical Design Process');
#33251=PRODUCT_CONTEXT('part definition',#33250,'mechanical');
#33269=PRODUCT('P_Torque Wrench_Pivot Cube_PRT-TQ-1012-07_M_Rev00',
'PRT-TQ-1012-07',$,(#33251));
#33288=PRESENTATION_STYLE_ASSIGNMENT((#33295));
#33295=SURFACE_STYLE_USAGE(.BOTH.,#33302);
#33302=SURFACE_SIDE_STYLE('',(#33309));
#33309=SURFACE_STYLE_FILL_AREA(#33316);
#33316=FILL_AREA_STYLE('Opaque(192,192,192)',(#33323));
#33323=FILL_AREA_STYLE_COLOUR('Opaque(192,192,192)',#33330);
#33330=COLOUR_RGB('Opaque(192,192,192)', 0.72549020, 0.75294118, 0.79215686);
ENDSEC;
END-ISO-10303-21;
